ISO-10303-21;
HEADER;
/* Generated by software containing ST-Developer
 * from STEP Tools, Inc. (www.steptools.com) 
 */

FILE_DESCRIPTION(
/* description */ (''),
/* implementation_level */ '2;1');

FILE_NAME(
/* name */ '13_Cotter_Pin_5-32x1-1-4.step',
/* time_stamp */ '2026-10-25T01:26:34-07:00',
/* author */ (''),
/* organization */ (''),
/* preprocessor_version */ 'ST-DEVELOPER v20.2',
/* originating_system */ 'Autodesk Translation Framework v15.15.0.0',
/* authorisation */ '');

FILE_SCHEMA (('AUTOMOTIVE_DESIGN { 1 0 10303 214 3 1 1 }'));
ENDSEC;

DATA;
#10=MECHANICAL_DESIGN_GEOMETRIC_PRESENTATION_REPRESENTATION('',(#330),#71628);
#180=TOROIDAL_SURFACE('',#37211,2.29999999999999,0.999999999999996);
#263=(
BOUNDED_CURVE()
B_SPLINE_CURVE(2,(#62887,#62888,#62889),.UNSPECIFIED.,.F.,.F.)
B_SPLINE_CURVE_WITH_KNOTS((3,3),(0.0543046845342199,0.0689123358693617),
 .UNSPECIFIED.)
CURVE()
GEOMETRIC_REPRESENTATION_ITEM()
RATIONAL_B_SPLINE_CURVE((1.00437382539668,1.00277520786002,1.00000007127116))
REPRESENTATION_ITEM('')
);
#264=(
BOUNDED_CURVE()
B_SPLINE_CURVE(2,(#62908,#62909,#62910),.UNSPECIFIED.,.F.,.F.)
B_SPLINE_CURVE_WITH_KNOTS((3,3),(1.87576610016924E-7,0.0146078389114927),
 .UNSPECIFIED.)
CURVE()
GEOMETRIC_REPRESENTATION_ITEM()
RATIONAL_B_SPLINE_CURVE((1.00000007127116,1.00277520785907,1.00437382539519))
REPRESENTATION_ITEM('')
);
#265=(
BOUNDED_CURVE()
B_SPLINE_CURVE(2,(#62927,#62928,#62929),.UNSPECIFIED.,.F.,.F.)
B_SPLINE_CURVE_WITH_KNOTS((3,3),(1.87576606599038E-7,0.0146078389114552),
 .UNSPECIFIED.)
CURVE()
GEOMETRIC_REPRESENTATION_ITEM()
RATIONAL_B_SPLINE_CURVE((1.00000007127116,1.00277520785998,1.00437382539664))
REPRESENTATION_ITEM('')
);
#266=(
BOUNDED_CURVE()
B_SPLINE_CURVE(2,(#62951,#62952,#62953),.UNSPECIFIED.,.F.,.F.)
B_SPLINE_CURVE_WITH_KNOTS((3,3),(0.0543046845342203,0.0689123358693609),
 .UNSPECIFIED.)
CURVE()
GEOMETRIC_REPRESENTATION_ITEM()
RATIONAL_B_SPLINE_CURVE((1.0043738253967,1.00277520786004,1.00000007127116))
REPRESENTATION_ITEM('')
);
#304=SHAPE_REPRESENTATION_RELATIONSHIP('SRR','None',#71692,#317);
#317=ADVANCED_BREP_SHAPE_REPRESENTATION('',(#343),#71624);
#330=STYLED_ITEM('',(#71818),#343);
#343=MANIFOLD_SOLID_BREP('Body1',#34217);
#674=B_SPLINE_CURVE_WITH_KNOTS('',3,(#62831,#62832,#62833,#62834,#62835,
#62836),.UNSPECIFIED.,.F.,.F.,(4,2,4),(-0.0699398717026881,-0.0424031601887617,
-0.0310509275685648),.UNSPECIFIED.);
#675=B_SPLINE_CURVE_WITH_KNOTS('',3,(#62842,#62843,#62844,#62845,#62846,
#62847),.UNSPECIFIED.,.F.,.F.,(4,2,4),(-0.0581997287702625,-0.0419989606450143,
-0.0194152449888361),.UNSPECIFIED.);
#676=B_SPLINE_CURVE_WITH_KNOTS('',3,(#62850,#62851,#62852,#62853,#62854,
#62855,#62856,#62857,#62858,#62859,#62860,#62861,#62862,#62863,#62864,#62865),
 .UNSPECIFIED.,.F.,.F.,(4,2,2,2,2,2,2,4),(0.0233074596666565,0.0349077749662999,
0.0719158476770912,0.110933651903281,0.149781045314824,0.188810000879272,
0.217148839309655,0.222449805752671),.UNSPECIFIED.);
#677=B_SPLINE_CURVE_WITH_KNOTS('',3,(#62897,#62898,#62899,#62900),
 .UNSPECIFIED.,.F.,.F.,(4,4),(0.0179911303970816,0.0747141480456938),
 .UNSPECIFIED.);
#678=B_SPLINE_CURVE_WITH_KNOTS('',3,(#62904,#62905,#62906,#62907),
 .UNSPECIFIED.,.F.,.F.,(4,4),(0.0179911303970802,0.0747141480456902),
 .UNSPECIFIED.);
#679=B_SPLINE_CURVE_WITH_KNOTS('',3,(#62938,#62939,#62940,#62941),
 .UNSPECIFIED.,.F.,.F.,(4,4),(0.,0.0567455036329469),.UNSPECIFIED.);
#680=B_SPLINE_CURVE_WITH_KNOTS('',3,(#62945,#62946,#62947,#62948),
 .UNSPECIFIED.,.F.,.F.,(4,4),(0.0179911303970801,0.0747141480456939),
 .UNSPECIFIED.);
#681=B_SPLINE_CURVE_WITH_KNOTS('',3,(#62966,#62967,#62968,#62969,#62970,
#62971,#62972,#62973,#62974,#62975,#62976,#62977,#62978,#62979,#62980,#62981,
#62982,#62983,#62984,#62985,#62986,#62987,#62988),.UNSPECIFIED.,.F.,.F.,
(4,2,2,2,2,2,2,2,2,3,4),(-0.598135905708757,-0.517314332218455,-0.362696133580663,
-0.318209117763193,-0.286159070534776,-0.258657166109227,-0.231155261683679,
-0.199105214455262,-0.154618198637792,0.,0.0808215734903014),
 .UNSPECIFIED.);
#1293=FACE_BOUND('',#7196,.T.);
#2789=PLANE('',#37196);
#2790=PLANE('',#37199);
#2791=PLANE('',#37200);
#2792=PLANE('',#37201);
#2793=PLANE('',#37202);
#2794=PLANE('',#37203);
#2795=PLANE('',#37204);
#2796=PLANE('',#37205);
#2797=PLANE('',#37206);
#2798=PLANE('',#37209);
#2799=PLANE('',#37210);
#2800=PLANE('',#37214);
#3071=CYLINDRICAL_SURFACE('',#37190,1.95);
#4922=FACE_OUTER_BOUND('',#7180,.T.);
#4923=FACE_OUTER_BOUND('',#7181,.T.);
#4924=FACE_OUTER_BOUND('',#7182,.T.);
#4925=FACE_OUTER_BOUND('',#7183,.T.);
#4926=FACE_OUTER_BOUND('',#7184,.T.);
#4927=FACE_OUTER_BOUND('',#7185,.T.);
#4928=FACE_OUTER_BOUND('',#7186,.T.);
#4929=FACE_OUTER_BOUND('',#7187,.T.);
#4930=FACE_OUTER_BOUND('',#7188,.T.);
#4931=FACE_OUTER_BOUND('',#7189,.T.);
#4932=FACE_OUTER_BOUND('',#7190,.T.);
#4933=FACE_OUTER_BOUND('',#7191,.T.);
#4934=FACE_OUTER_BOUND('',#7192,.T.);
#4935=FACE_OUTER_BOUND('',#7193,.T.);
#4936=FACE_OUTER_BOUND('',#7194,.T.);
#4937=FACE_OUTER_BOUND('',#7195,.T.);
#4938=FACE_OUTER_BOUND('',#7197,.T.);
#7180=EDGE_LOOP('',(#30432,#30433,#30434,#30435,#30436));
#7181=EDGE_LOOP('',(#30437,#30438,#30439,#30440,#30441,#30442,#30443,#30444,
#30445,#30446,#30447,#30448,#30449,#30450));
#7182=EDGE_LOOP('',(#30451,#30452,#30453,#30454,#30455));
#7183=EDGE_LOOP('',(#30456,#30457,#30458,#30459,#30460,#30461));
#7184=EDGE_LOOP('',(#30462,#30463,#30464,#30465,#30466,#30467));
#7185=EDGE_LOOP('',(#30468,#30469,#30470,#30471));
#7186=EDGE_LOOP('',(#30472,#30473,#30474,#30475,#30476));
#7187=EDGE_LOOP('',(#30477,#30478,#30479,#30480));
#7188=EDGE_LOOP('',(#30481,#30482,#30483,#30484,#30485,#30486));
#7189=EDGE_LOOP('',(#30487,#30488,#30489,#30490,#30491));
#7190=EDGE_LOOP('',(#30492,#30493,#30494,#30495,#30496));
#7191=EDGE_LOOP('',(#30497,#30498));
#7192=EDGE_LOOP('',(#30499,#30500,#30501,#30502,#30503,#30504));
#7193=EDGE_LOOP('',(#30505,#30506));
#7194=EDGE_LOOP('',(#30507,#30508,#30509,#30510,#30511,#30512,#30513,#30514,
#30515));
#7195=EDGE_LOOP('',(#30516,#30517,#30518,#30519));
#7196=EDGE_LOOP('',(#30520,#30521,#30522,#30523));
#7197=EDGE_LOOP('',(#30524,#30525));
#10163=LINE('',#62867,#13213);
#10164=LINE('',#62871,#13214);
#10165=LINE('',#62875,#13215);
#10166=LINE('',#62879,#13216);
#10167=LINE('',#62883,#13217);
#10168=LINE('',#62891,#13218);
#10169=LINE('',#62893,#13219);
#10170=LINE('',#62894,#13220);
#10171=LINE('',#62913,#13221);
#10172=LINE('',#62914,#13222);
#10173=LINE('',#62915,#13223);
#10174=LINE('',#62918,#13224);
#10175=LINE('',#62919,#13225);
#10176=LINE('',#62923,#13226);
#10177=LINE('',#62925,#13227);
#10178=LINE('',#62926,#13228);
#10179=LINE('',#62932,#13229);
#10180=LINE('',#62934,#13230);
#10181=LINE('',#62935,#13231);
#10182=LINE('',#62943,#13232);
#10183=LINE('',#62949,#13233);
#10184=LINE('',#62954,#13234);
#10185=LINE('',#62956,#13235);
#13213=VECTOR('',#45942,1.95);
#13214=VECTOR('',#45945,10.);
#13215=VECTOR('',#45948,10.);
#13216=VECTOR('',#45951,10.);
#13217=VECTOR('',#45954,10.);
#13218=VECTOR('',#45959,10.);
#13219=VECTOR('',#45960,10.);
#13220=VECTOR('',#45961,10.);
#13221=VECTOR('',#45968,10.);
#13222=VECTOR('',#45969,10.);
#13223=VECTOR('',#45970,10.);
#13224=VECTOR('',#45973,10.);
#13225=VECTOR('',#45974,10.);
#13226=VECTOR('',#45977,10.);
#13227=VECTOR('',#45978,10.);
#13228=VECTOR('',#45979,10.);
#13229=VECTOR('',#45982,10.);
#13230=VECTOR('',#45983,10.);
#13231=VECTOR('',#45984,10.);
#13232=VECTOR('',#45987,10.);
#13233=VECTOR('',#45988,10.);
#13234=VECTOR('',#45991,10.);
#13235=VECTOR('',#45994,10.);
#14385=CIRCLE('',#37187,1.95);
#14386=CIRCLE('',#37188,1.95);
#14387=CIRCLE('',#37189,1.75);
#14388=CIRCLE('',#37191,1.95);
#14389=CIRCLE('',#37192,1.95);
#14390=CIRCLE('',#37193,1.95);
#14391=CIRCLE('',#37194,1.95);
#14392=CIRCLE('',#37195,1.95);
#14393=CIRCLE('',#37198,1.55000000000001);
#14394=CIRCLE('',#37208,1.55000000000001);
#14395=CIRCLE('',#37212,0.999999999999996);
#14396=CIRCLE('',#37213,1.29999999999999);
#16971=VERTEX_POINT('',#62829);
#16972=VERTEX_POINT('',#62830);
#16973=VERTEX_POINT('',#62837);
#16974=VERTEX_POINT('',#62839);
#16975=VERTEX_POINT('',#62841);
#16976=VERTEX_POINT('',#62866);
#16977=VERTEX_POINT('',#62868);
#16978=VERTEX_POINT('',#62870);
#16979=VERTEX_POINT('',#62872);
#16980=VERTEX_POINT('',#62874);
#16981=VERTEX_POINT('',#62876);
#16982=VERTEX_POINT('',#62878);
#16983=VERTEX_POINT('',#62880);
#16984=VERTEX_POINT('',#62882);
#16985=VERTEX_POINT('',#62886);
#16986=VERTEX_POINT('',#62890);
#16987=VERTEX_POINT('',#62892);
#16988=VERTEX_POINT('',#62896);
#16989=VERTEX_POINT('',#62901);
#16990=VERTEX_POINT('',#62903);
#16991=VERTEX_POINT('',#62912);
#16992=VERTEX_POINT('',#62917);
#16993=VERTEX_POINT('',#62921);
#16994=VERTEX_POINT('',#62922);
#16995=VERTEX_POINT('',#62924);
#16996=VERTEX_POINT('',#62931);
#16997=VERTEX_POINT('',#62933);
#16998=VERTEX_POINT('',#62937);
#16999=VERTEX_POINT('',#62942);
#17000=VERTEX_POINT('',#62944);
#17001=VERTEX_POINT('',#62963);
#21530=EDGE_CURVE('',#16971,#16972,#674,.F.);
#21531=EDGE_CURVE('',#16972,#16973,#14385,.T.);
#21532=EDGE_CURVE('',#16973,#16974,#14386,.T.);
#21533=EDGE_CURVE('',#16974,#16975,#675,.F.);
#21534=EDGE_CURVE('',#16975,#16971,#14387,.T.);
#21535=EDGE_CURVE('',#16972,#16974,#676,.T.);
#21536=EDGE_CURVE('',#16973,#16976,#10163,.T.);
#21537=EDGE_CURVE('',#16976,#16977,#14388,.T.);
#21538=EDGE_CURVE('',#16978,#16977,#10164,.T.);
#21539=EDGE_CURVE('',#16979,#16978,#14389,.T.);
#21540=EDGE_CURVE('',#16980,#16979,#10165,.T.);
#21541=EDGE_CURVE('',#16980,#16981,#14390,.T.);
#21542=EDGE_CURVE('',#16982,#16981,#10166,.T.);
#21543=EDGE_CURVE('',#16983,#16982,#14391,.T.);
#21544=EDGE_CURVE('',#16984,#16983,#10167,.T.);
#21545=EDGE_CURVE('',#16984,#16976,#14392,.T.);
#21546=EDGE_CURVE('',#16985,#16978,#263,.T.);
#21547=EDGE_CURVE('',#16977,#16986,#10168,.F.);
#21548=EDGE_CURVE('',#16986,#16987,#10169,.T.);
#21549=EDGE_CURVE('',#16987,#16985,#10170,.T.);
#21550=EDGE_CURVE('',#16985,#16988,#677,.T.);
#21551=EDGE_CURVE('',#16988,#16989,#14393,.T.);
#21552=EDGE_CURVE('',#16990,#16989,#678,.T.);
#21553=EDGE_CURVE('',#16979,#16990,#264,.T.);
#21554=EDGE_CURVE('',#16987,#16991,#10171,.T.);
#21555=EDGE_CURVE('',#16990,#16991,#10172,.T.);
#21556=EDGE_CURVE('',#16989,#16988,#10173,.T.);
#21557=EDGE_CURVE('',#16986,#16992,#10174,.T.);
#21558=EDGE_CURVE('',#16991,#16992,#10175,.T.);
#21559=EDGE_CURVE('',#16993,#16994,#10176,.T.);
#21560=EDGE_CURVE('',#16994,#16995,#10177,.T.);
#21561=EDGE_CURVE('',#16995,#16984,#10178,.F.);
#21562=EDGE_CURVE('',#16983,#16993,#265,.T.);
#21563=EDGE_CURVE('',#16996,#16994,#10179,.T.);
#21564=EDGE_CURVE('',#16997,#16996,#10180,.T.);
#21565=EDGE_CURVE('',#16997,#16995,#10181,.T.);
#21566=EDGE_CURVE('',#16998,#16993,#679,.T.);
#21567=EDGE_CURVE('',#16998,#16999,#10182,.T.);
#21568=EDGE_CURVE('',#17000,#16999,#680,.T.);
#21569=EDGE_CURVE('',#16996,#17000,#10183,.T.);
#21570=EDGE_CURVE('',#17000,#16982,#266,.T.);
#21571=EDGE_CURVE('',#16981,#16997,#10184,.F.);
#21572=EDGE_CURVE('',#16992,#16980,#10185,.F.);
#21573=EDGE_CURVE('',#16999,#16998,#14394,.T.);
#21574=EDGE_CURVE('',#17001,#17001,#14395,.T.);
#21575=EDGE_CURVE('',#17001,#17001,#14396,.T.);
#21576=EDGE_CURVE('',#16975,#16971,#681,.T.);
#30432=ORIENTED_EDGE('',*,*,#21530,.T.);
#30433=ORIENTED_EDGE('',*,*,#21531,.T.);
#30434=ORIENTED_EDGE('',*,*,#21532,.T.);
#30435=ORIENTED_EDGE('',*,*,#21533,.T.);
#30436=ORIENTED_EDGE('',*,*,#21534,.T.);
#30437=ORIENTED_EDGE('',*,*,#21531,.F.);
#30438=ORIENTED_EDGE('',*,*,#21535,.T.);
#30439=ORIENTED_EDGE('',*,*,#21532,.F.);
#30440=ORIENTED_EDGE('',*,*,#21536,.T.);
#30441=ORIENTED_EDGE('',*,*,#21537,.T.);
#30442=ORIENTED_EDGE('',*,*,#21538,.F.);
#30443=ORIENTED_EDGE('',*,*,#21539,.F.);
#30444=ORIENTED_EDGE('',*,*,#21540,.F.);
#30445=ORIENTED_EDGE('',*,*,#21541,.T.);
#30446=ORIENTED_EDGE('',*,*,#21542,.F.);
#30447=ORIENTED_EDGE('',*,*,#21543,.F.);
#30448=ORIENTED_EDGE('',*,*,#21544,.F.);
#30449=ORIENTED_EDGE('',*,*,#21545,.T.);
#30450=ORIENTED_EDGE('',*,*,#21536,.F.);
#30451=ORIENTED_EDGE('',*,*,#21546,.T.);
#30452=ORIENTED_EDGE('',*,*,#21538,.T.);
#30453=ORIENTED_EDGE('',*,*,#21547,.T.);
#30454=ORIENTED_EDGE('',*,*,#21548,.T.);
#30455=ORIENTED_EDGE('',*,*,#21549,.T.);
#30456=ORIENTED_EDGE('',*,*,#21546,.F.);
#30457=ORIENTED_EDGE('',*,*,#21550,.T.);
#30458=ORIENTED_EDGE('',*,*,#21551,.T.);
#30459=ORIENTED_EDGE('',*,*,#21552,.F.);
#30460=ORIENTED_EDGE('',*,*,#21553,.F.);
#30461=ORIENTED_EDGE('',*,*,#21539,.T.);
#30462=ORIENTED_EDGE('',*,*,#21549,.F.);
#30463=ORIENTED_EDGE('',*,*,#21554,.T.);
#30464=ORIENTED_EDGE('',*,*,#21555,.F.);
#30465=ORIENTED_EDGE('',*,*,#21552,.T.);
#30466=ORIENTED_EDGE('',*,*,#21556,.T.);
#30467=ORIENTED_EDGE('',*,*,#21550,.F.);
#30468=ORIENTED_EDGE('',*,*,#21548,.F.);
#30469=ORIENTED_EDGE('',*,*,#21557,.T.);
#30470=ORIENTED_EDGE('',*,*,#21558,.F.);
#30471=ORIENTED_EDGE('',*,*,#21554,.F.);
#30472=ORIENTED_EDGE('',*,*,#21559,.T.);
#30473=ORIENTED_EDGE('',*,*,#21560,.T.);
#30474=ORIENTED_EDGE('',*,*,#21561,.T.);
#30475=ORIENTED_EDGE('',*,*,#21544,.T.);
#30476=ORIENTED_EDGE('',*,*,#21562,.T.);
#30477=ORIENTED_EDGE('',*,*,#21560,.F.);
#30478=ORIENTED_EDGE('',*,*,#21563,.F.);
#30479=ORIENTED_EDGE('',*,*,#21564,.F.);
#30480=ORIENTED_EDGE('',*,*,#21565,.T.);
#30481=ORIENTED_EDGE('',*,*,#21559,.F.);
#30482=ORIENTED_EDGE('',*,*,#21566,.F.);
#30483=ORIENTED_EDGE('',*,*,#21567,.T.);
#30484=ORIENTED_EDGE('',*,*,#21568,.F.);
#30485=ORIENTED_EDGE('',*,*,#21569,.F.);
#30486=ORIENTED_EDGE('',*,*,#21563,.T.);
#30487=ORIENTED_EDGE('',*,*,#21570,.T.);
#30488=ORIENTED_EDGE('',*,*,#21542,.T.);
#30489=ORIENTED_EDGE('',*,*,#21571,.T.);
#30490=ORIENTED_EDGE('',*,*,#21564,.T.);
#30491=ORIENTED_EDGE('',*,*,#21569,.T.);
#30492=ORIENTED_EDGE('',*,*,#21555,.T.);
#30493=ORIENTED_EDGE('',*,*,#21558,.T.);
#30494=ORIENTED_EDGE('',*,*,#21572,.T.);
#30495=ORIENTED_EDGE('',*,*,#21540,.T.);
#30496=ORIENTED_EDGE('',*,*,#21553,.T.);
#30497=ORIENTED_EDGE('',*,*,#21551,.F.);
#30498=ORIENTED_EDGE('',*,*,#21556,.F.);
#30499=ORIENTED_EDGE('',*,*,#21562,.F.);
#30500=ORIENTED_EDGE('',*,*,#21543,.T.);
#30501=ORIENTED_EDGE('',*,*,#21570,.F.);
#30502=ORIENTED_EDGE('',*,*,#21568,.T.);
#30503=ORIENTED_EDGE('',*,*,#21573,.T.);
#30504=ORIENTED_EDGE('',*,*,#21566,.T.);
#30505=ORIENTED_EDGE('',*,*,#21573,.F.);
#30506=ORIENTED_EDGE('',*,*,#21567,.F.);
#30507=ORIENTED_EDGE('',*,*,#21541,.F.);
#30508=ORIENTED_EDGE('',*,*,#21572,.F.);
#30509=ORIENTED_EDGE('',*,*,#21557,.F.);
#30510=ORIENTED_EDGE('',*,*,#21547,.F.);
#30511=ORIENTED_EDGE('',*,*,#21537,.F.);
#30512=ORIENTED_EDGE('',*,*,#21545,.F.);
#30513=ORIENTED_EDGE('',*,*,#21561,.F.);
#30514=ORIENTED_EDGE('',*,*,#21565,.F.);
#30515=ORIENTED_EDGE('',*,*,#21571,.F.);
#30516=ORIENTED_EDGE('',*,*,#21574,.F.);
#30517=ORIENTED_EDGE('',*,*,#21575,.T.);
#30518=ORIENTED_EDGE('',*,*,#21574,.T.);
#30519=ORIENTED_EDGE('',*,*,#21575,.F.);
#30520=ORIENTED_EDGE('',*,*,#21576,.F.);
#30521=ORIENTED_EDGE('',*,*,#21533,.F.);
#30522=ORIENTED_EDGE('',*,*,#21535,.F.);
#30523=ORIENTED_EDGE('',*,*,#21530,.F.);
#30524=ORIENTED_EDGE('',*,*,#21534,.F.);
#30525=ORIENTED_EDGE('',*,*,#21576,.T.);
#32081=CONICAL_SURFACE('',#37186,1.85,0.785398163397437);
#32082=CONICAL_SURFACE('',#37197,1.75,0.785398163397437);
#32083=CONICAL_SURFACE('',#37207,1.75,0.785398163397437);
#33896=ADVANCED_FACE('',(#4922),#32081,.T.);
#33897=ADVANCED_FACE('',(#4923),#3071,.T.);
#33898=ADVANCED_FACE('',(#4924),#2789,.T.);
#33899=ADVANCED_FACE('',(#4925),#32082,.T.);
#33900=ADVANCED_FACE('',(#4926),#2790,.T.);
#33901=ADVANCED_FACE('',(#4927),#2791,.F.);
#33902=ADVANCED_FACE('',(#4928),#2792,.T.);
#33903=ADVANCED_FACE('',(#4929),#2793,.F.);
#33904=ADVANCED_FACE('',(#4930),#2794,.T.);
#33905=ADVANCED_FACE('',(#4931),#2795,.T.);
#33906=ADVANCED_FACE('',(#4932),#2796,.T.);
#33907=ADVANCED_FACE('',(#4933),#2797,.F.);
#33908=ADVANCED_FACE('',(#4934),#32083,.T.);
#33909=ADVANCED_FACE('',(#4935),#2798,.F.);
#33910=ADVANCED_FACE('',(#4936),#2799,.F.);
#33911=ADVANCED_FACE('',(#4937,#1293),#180,.T.);
#33912=ADVANCED_FACE('',(#4938),#2800,.T.);
#34217=CLOSED_SHELL('',(#33896,#33897,#33898,#33899,#33900,#33901,#33902,
#33903,#33904,#33905,#33906,#33907,#33908,#33909,#33910,#33911,#33912));
#37185=AXIS2_PLACEMENT_3D('',#62827,#45930,#45931);
#37186=AXIS2_PLACEMENT_3D('',#62828,#45932,#45933);
#37187=AXIS2_PLACEMENT_3D('',#62838,#45934,#45935);
#37188=AXIS2_PLACEMENT_3D('',#62840,#45936,#45937);
#37189=AXIS2_PLACEMENT_3D('',#62848,#45938,#45939);
#37190=AXIS2_PLACEMENT_3D('',#62849,#45940,#45941);
#37191=AXIS2_PLACEMENT_3D('',#62869,#45943,#45944);
#37192=AXIS2_PLACEMENT_3D('',#62873,#45946,#45947);
#37193=AXIS2_PLACEMENT_3D('',#62877,#45949,#45950);
#37194=AXIS2_PLACEMENT_3D('',#62881,#45952,#45953);
#37195=AXIS2_PLACEMENT_3D('',#62884,#45955,#45956);
#37196=AXIS2_PLACEMENT_3D('',#62885,#45957,#45958);
#37197=AXIS2_PLACEMENT_3D('',#62895,#45962,#45963);
#37198=AXIS2_PLACEMENT_3D('',#62902,#45964,#45965);
#37199=AXIS2_PLACEMENT_3D('',#62911,#45966,#45967);
#37200=AXIS2_PLACEMENT_3D('',#62916,#45971,#45972);
#37201=AXIS2_PLACEMENT_3D('',#62920,#45975,#45976);
#37202=AXIS2_PLACEMENT_3D('',#62930,#45980,#45981);
#37203=AXIS2_PLACEMENT_3D('',#62936,#45985,#45986);
#37204=AXIS2_PLACEMENT_3D('',#62950,#45989,#45990);
#37205=AXIS2_PLACEMENT_3D('',#62955,#45992,#45993);
#37206=AXIS2_PLACEMENT_3D('',#62957,#45995,#45996);
#37207=AXIS2_PLACEMENT_3D('',#62958,#45997,#45998);
#37208=AXIS2_PLACEMENT_3D('',#62959,#45999,#46000);
#37209=AXIS2_PLACEMENT_3D('',#62960,#46001,#46002);
#37210=AXIS2_PLACEMENT_3D('',#62961,#46003,#46004);
#37211=AXIS2_PLACEMENT_3D('',#62962,#46005,#46006);
#37212=AXIS2_PLACEMENT_3D('',#62964,#46007,#46008);
#37213=AXIS2_PLACEMENT_3D('',#62965,#46009,#46010);
#37214=AXIS2_PLACEMENT_3D('',#62989,#46011,#46012);
#45930=DIRECTION('axis',(0.,0.,1.));
#45931=DIRECTION('refdir',(1.,0.,0.));
#45932=DIRECTION('center_axis',(0.,0.,-1.));
#45933=DIRECTION('ref_axis',(-1.,-9.30527706900849E-13,0.));
#45934=DIRECTION('center_axis',(0.,0.,1.));
#45935=DIRECTION('ref_axis',(-2.22044604925031E-16,1.,0.));
#45936=DIRECTION('center_axis',(0.,0.,1.));
#45937=DIRECTION('ref_axis',(-2.22044604925031E-16,1.,0.));
#45938=DIRECTION('center_axis',(0.,0.,-1.));
#45939=DIRECTION('ref_axis',(-2.22044604925031E-16,1.,0.));
#45940=DIRECTION('center_axis',(0.,0.,1.));
#45941=DIRECTION('ref_axis',(-2.22044604925031E-16,1.,0.));
#45942=DIRECTION('',(0.,0.,-1.));
#45943=DIRECTION('center_axis',(0.,0.,1.));
#45944=DIRECTION('ref_axis',(-2.22044604925031E-16,1.,0.));
#45945=DIRECTION('',(0.,0.,1.));
#45946=DIRECTION('center_axis',(0.,0.,-1.));
#45947=DIRECTION('ref_axis',(-2.22044604925031E-16,1.,0.));
#45948=DIRECTION('',(0.,0.,-1.));
#45949=DIRECTION('center_axis',(0.,0.,1.));
#45950=DIRECTION('ref_axis',(-2.22044604925031E-16,1.,0.));
#45951=DIRECTION('',(0.,0.,1.));
#45952=DIRECTION('center_axis',(0.,0.,-1.));
#45953=DIRECTION('ref_axis',(-2.22044604925031E-16,1.,0.));
#45954=DIRECTION('',(0.,0.,-1.));
#45955=DIRECTION('center_axis',(0.,0.,1.));
#45956=DIRECTION('ref_axis',(-2.22044604925031E-16,1.,0.));
#45957=DIRECTION('center_axis',(-0.660321146702944,-0.750983344167439,0.));
#45958=DIRECTION('ref_axis',(0.,0.,1.));
#45959=DIRECTION('',(0.750983344167439,-0.660321146702944,0.));
#45960=DIRECTION('',(0.,0.,-1.));
#45961=DIRECTION('',(0.600503115876144,-0.528007590519368,-0.600503115876158));
#45962=DIRECTION('center_axis',(0.,0.,1.));
#45963=DIRECTION('ref_axis',(-2.22044604925031E-16,1.,0.));
#45964=DIRECTION('center_axis',(0.,0.,1.));
#45965=DIRECTION('ref_axis',(-2.22044604925031E-16,1.,0.));
#45966=DIRECTION('center_axis',(-0.707106781186555,0.,-0.70710678118654));
#45967=DIRECTION('ref_axis',(-0.70710678118654,0.,0.707106781186555));
#45968=DIRECTION('',(0.,1.,0.));
#45969=DIRECTION('',(-0.600503115876144,-0.528007590519368,0.600503115876158));
#45970=DIRECTION('',(0.,-1.,0.));
#45971=DIRECTION('center_axis',(1.,0.,0.));
#45972=DIRECTION('ref_axis',(0.,0.,-1.));
#45973=DIRECTION('',(0.,1.,0.));
#45974=DIRECTION('',(0.,0.,1.));
#45975=DIRECTION('center_axis',(0.660321146702944,-0.750983344167439,0.));
#45976=DIRECTION('ref_axis',(0.,0.,-1.));
#45977=DIRECTION('',(0.600503115876144,0.528007590519368,0.600503115876158));
#45978=DIRECTION('',(0.,0.,1.));
#45979=DIRECTION('',(0.750983344167439,0.660321146702944,0.));
#45980=DIRECTION('center_axis',(-1.,0.,0.));
#45981=DIRECTION('ref_axis',(0.,0.,1.));
#45982=DIRECTION('',(0.,-1.,0.));
#45983=DIRECTION('',(0.,0.,-1.));
#45984=DIRECTION('',(0.,-1.,0.));
#45985=DIRECTION('center_axis',(0.707106781186555,0.,-0.70710678118654));
#45986=DIRECTION('ref_axis',(-0.70710678118654,0.,-0.707106781186555));
#45987=DIRECTION('',(0.,1.,0.));
#45988=DIRECTION('',(-0.600503115876144,0.528007590519368,-0.600503115876158));
#45989=DIRECTION('center_axis',(0.660321146702944,0.750983344167439,0.));
#45990=DIRECTION('ref_axis',(0.,0.,-1.));
#45991=DIRECTION('',(-0.750983344167439,0.660321146702944,0.));
#45992=DIRECTION('center_axis',(-0.660321146702944,0.750983344167439,0.));
#45993=DIRECTION('ref_axis',(0.,0.,1.));
#45994=DIRECTION('',(-0.750983344167439,-0.660321146702944,0.));
#45995=DIRECTION('center_axis',(0.,0.,1.));
#45996=DIRECTION('ref_axis',(-2.22044604925031E-16,1.,0.));
#45997=DIRECTION('center_axis',(0.,0.,1.));
#45998=DIRECTION('ref_axis',(-2.22044604925031E-16,1.,0.));
#45999=DIRECTION('center_axis',(0.,0.,1.));
#46000=DIRECTION('ref_axis',(-2.22044604925031E-16,1.,0.));
#46001=DIRECTION('center_axis',(0.,0.,1.));
#46002=DIRECTION('ref_axis',(-2.22044604925031E-16,1.,0.));
#46003=DIRECTION('center_axis',(0.,0.,1.));
#46004=DIRECTION('ref_axis',(1.,0.,0.));
#46005=DIRECTION('center_axis',(0.,-1.,0.));
#46006=DIRECTION('ref_axis',(0.,0.,-1.));
#46007=DIRECTION('center_axis',(-1.,0.,0.));
#46008=DIRECTION('ref_axis',(0.,0.,1.));
#46009=DIRECTION('center_axis',(0.,1.,0.));
#46010=DIRECTION('ref_axis',(0.,0.,-1.));
#46011=DIRECTION('center_axis',(0.,0.,1.));
#46012=DIRECTION('ref_axis',(-2.22044604925031E-16,1.,0.));
#62827=CARTESIAN_POINT('',(0.,0.,0.));
#62828=CARTESIAN_POINT('Origin',(109.5,0.,17.1));
#62829=CARTESIAN_POINT('',(110.957496466156,0.968609344154195,17.2));
#62830=CARTESIAN_POINT('',(111.26134813329,0.836751309143921,17.0000000000042));
#62831=CARTESIAN_POINT('Ctrl Pts',(111.261348133289,0.836751309140648,17.0000000000024));
#62832=CARTESIAN_POINT('Ctrl Pts',(111.193368852489,0.880393938856773,17.0426754624596));
#62833=CARTESIAN_POINT('Ctrl Pts',(111.121707329493,0.915065044515368,17.088908703297));
#62834=CARTESIAN_POINT('Ctrl Pts',(111.018383164403,0.951678216844113,17.1581953291081));
#62835=CARTESIAN_POINT('Ctrl Pts',(110.987987650589,0.960873765425233,17.1788868315244));
#62836=CARTESIAN_POINT('Ctrl Pts',(110.957496464733,0.968609345524605,17.1999999974435));
#62837=CARTESIAN_POINT('',(109.5,-1.95,17.0000000000057));
#62838=CARTESIAN_POINT('Origin',(109.5,0.,17.));
#62839=CARTESIAN_POINT('',(111.261348133293,-0.836751309138393,17.0000000000001));
#62840=CARTESIAN_POINT('Origin',(109.5,0.,17.));
#62841=CARTESIAN_POINT('',(110.957496466156,-0.968609344154194,17.2));
#62842=CARTESIAN_POINT('Ctrl Pts',(110.957496464733,-0.968609345524603,
17.1999999974435));
#62843=CARTESIAN_POINT('Ctrl Pts',(111.001101495698,-0.957546797437459,
17.1698063454805));
#62844=CARTESIAN_POINT('Ctrl Pts',(111.044512077677,-0.943498238918733,
17.1404742731241));
#62845=CARTESIAN_POINT('Ctrl Pts',(111.147005642954,-0.902487957738779,
17.0726239093433));
#62846=CARTESIAN_POINT('Ctrl Pts',(111.20542520737,-0.872653771182455,17.0351068251626));
#62847=CARTESIAN_POINT('Ctrl Pts',(111.261348133292,-0.836751309139038,
17.0000000000008));
#62848=CARTESIAN_POINT('Origin',(109.5,0.,17.2));
#62849=CARTESIAN_POINT('Origin',(109.5,0.,-16.));
#62850=CARTESIAN_POINT('Ctrl Pts',(111.261348133291,0.836751309142101,17.0000000000057));
#62851=CARTESIAN_POINT('Ctrl Pts',(111.271270988545,0.815863857414333,16.9694752063524));
#62852=CARTESIAN_POINT('Ctrl Pts',(111.281647172364,0.79306554162572,16.9403253270067));
#62853=CARTESIAN_POINT('Ctrl Pts',(111.325941268158,0.689755334685708,16.8242697948987));
#62854=CARTESIAN_POINT('Ctrl Pts',(111.360584011539,0.594205474502249,16.7528911725506));
#62855=CARTESIAN_POINT('Ctrl Pts',(111.417556923573,0.37310394039917,16.643452411098));
#62856=CARTESIAN_POINT('Ctrl Pts',(111.438467087766,0.248212018892159,16.6083564739943));
#62857=CARTESIAN_POINT('Ctrl Pts',(111.454232282562,-0.00969172202381931,
16.5815554081639));
#62858=CARTESIAN_POINT('Ctrl Pts',(111.449047773732,-0.140002812849383,
16.5898935474965));
#62859=CARTESIAN_POINT('Ctrl Pts',(111.414723878012,-0.390345158053136,
16.6498762958916));
#62860=CARTESIAN_POINT('Ctrl Pts',(111.385873474846,-0.507644453415908,
16.7010984120851));
#62861=CARTESIAN_POINT('Ctrl Pts',(111.327369049441,-0.685129348563325,
16.8248010526809));
#62862=CARTESIAN_POINT('Ctrl Pts',(111.300518338828,-0.751237326031986,
16.887053403656));
#62863=CARTESIAN_POINT('Ctrl Pts',(111.270547957266,-0.817184329085975,
16.9722816702371));
#62864=CARTESIAN_POINT('Ctrl Pts',(111.265899036497,-0.827171730624058,
16.9860004628025));
#62865=CARTESIAN_POINT('Ctrl Pts',(111.261348133293,-0.836751309138331,
17.0000000000002));
#62866=CARTESIAN_POINT('',(109.5,-1.95,15.5));
#62867=CARTESIAN_POINT('',(109.5,-1.95,-16.));
#62868=CARTESIAN_POINT('',(109.84835607319,-1.9186318162356,15.5));
#62869=CARTESIAN_POINT('Origin',(109.5,0.,15.5));
#62870=CARTESIAN_POINT('',(109.84835607319,-1.9186318162356,-15.6));
#62871=CARTESIAN_POINT('',(109.84835607319,-1.9186318162356,-16.));
#62872=CARTESIAN_POINT('',(109.84835607319,1.9186318162356,-15.6));
#62873=CARTESIAN_POINT('Origin',(109.5,0.,-15.6));
#62874=CARTESIAN_POINT('',(109.84835607319,1.9186318162356,15.5));
#62875=CARTESIAN_POINT('',(109.84835607319,1.9186318162356,-16.));
#62876=CARTESIAN_POINT('',(109.15164392681,1.9186318162356,15.5));
#62877=CARTESIAN_POINT('Origin',(109.5,0.,15.5));
#62878=CARTESIAN_POINT('',(109.15164392681,1.9186318162356,-15.6));
#62879=CARTESIAN_POINT('',(109.15164392681,1.9186318162356,-16.));
#62880=CARTESIAN_POINT('',(109.15164392681,-1.9186318162356,-15.6));
#62881=CARTESIAN_POINT('Origin',(109.5,0.,-15.6));
#62882=CARTESIAN_POINT('',(109.15164392681,-1.9186318162356,15.5));
#62883=CARTESIAN_POINT('',(109.15164392681,-1.9186318162356,-16.));
#62884=CARTESIAN_POINT('Origin',(109.5,0.,15.5));
#62885=CARTESIAN_POINT('Origin',(109.749178036595,-1.83142701287898,-16.));
#62886=CARTESIAN_POINT('',(109.750434791609,-1.83253209412259,-15.7004347680384));
#62887=CARTESIAN_POINT('Ctrl Pts',(109.750434791609,-1.83253209412259,-15.7004347680384));
#62888=CARTESIAN_POINT('Ctrl Pts',(109.798101224611,-1.87444401393227,-15.6524546953631));
#62889=CARTESIAN_POINT('Ctrl Pts',(109.84835607319,-1.91863181623643,-15.5999999999986));
#62890=CARTESIAN_POINT('',(109.65,-1.74422220952236,15.5));
#62891=CARTESIAN_POINT('',(109.1825212855,-1.33317969677524,15.5));
#62892=CARTESIAN_POINT('',(109.65,-1.74422220952236,-15.6));
#62893=CARTESIAN_POINT('',(109.65,-1.74422220952236,-16.));
#62894=CARTESIAN_POINT('',(109.549428171904,-1.65579187964854,-15.4994281719038));
#62895=CARTESIAN_POINT('Origin',(109.5,0.,-15.8));
#62896=CARTESIAN_POINT('',(110.05,-1.44913767461895,-16.));
#62897=CARTESIAN_POINT('Ctrl Pts',(109.750434784424,-1.83253210215193,-15.7004347844244));
#62898=CARTESIAN_POINT('Ctrl Pts',(109.855124020005,-1.71256291063752,-15.8051240200051));
#62899=CARTESIAN_POINT('Ctrl Pts',(109.956584644308,-1.58450938593979,-15.9065846443083));
#62900=CARTESIAN_POINT('Ctrl Pts',(110.05,-1.44913767461895,-16.));
#62901=CARTESIAN_POINT('',(110.05,1.44913767461896,-16.));
#62902=CARTESIAN_POINT('Origin',(109.5,0.,-16.));
#62903=CARTESIAN_POINT('',(109.750434791609,1.83253209412259,-15.7004347680384));
#62904=CARTESIAN_POINT('Ctrl Pts',(109.750434784424,1.83253210215196,-15.7004347844244));
#62905=CARTESIAN_POINT('Ctrl Pts',(109.855124020005,1.71256291063753,-15.8051240200051));
#62906=CARTESIAN_POINT('Ctrl Pts',(109.956584644308,1.58450938593979,-15.9065846443083));
#62907=CARTESIAN_POINT('Ctrl Pts',(110.05,1.44913767461895,-16.));
#62908=CARTESIAN_POINT('Ctrl Pts',(109.84835607319,1.91863181623643,-15.5999999999986));
#62909=CARTESIAN_POINT('Ctrl Pts',(109.79810122461,1.87444401393154,-15.6524546953639));
#62910=CARTESIAN_POINT('Ctrl Pts',(109.750434791609,1.83253209412259,-15.7004347680384));
#62911=CARTESIAN_POINT('Origin',(109.85,0.,-15.8));
#62912=CARTESIAN_POINT('',(109.65,1.74422220952236,-15.6));
#62913=CARTESIAN_POINT('',(109.65,0.,-15.6));
#62914=CARTESIAN_POINT('',(109.549428171904,1.65579187964854,-15.4994281719038));
#62915=CARTESIAN_POINT('',(110.05,0.,-16.));
#62916=CARTESIAN_POINT('Origin',(109.65,0.,15.5));
#62917=CARTESIAN_POINT('',(109.65,1.74422220952236,15.5));
#62918=CARTESIAN_POINT('',(109.65,0.,15.5));
#62919=CARTESIAN_POINT('',(109.65,1.74422220952236,-16.));
#62920=CARTESIAN_POINT('Origin',(109.250821963405,-1.83142701287898,-16.));
#62921=CARTESIAN_POINT('',(109.249565208391,-1.83253209412259,-15.7004347680384));
#62922=CARTESIAN_POINT('',(109.35,-1.74422220952236,-15.6));
#62923=CARTESIAN_POINT('',(109.450571828096,-1.65579187964854,-15.4994281719038));
#62924=CARTESIAN_POINT('',(109.35,-1.74422220952236,15.5));
#62925=CARTESIAN_POINT('',(109.35,-1.74422220952236,-16.));
#62926=CARTESIAN_POINT('',(109.732882317017,-1.40756322422156,15.5));
#62927=CARTESIAN_POINT('Ctrl Pts',(109.15164392681,-1.91863181623643,-15.5999999999986));
#62928=CARTESIAN_POINT('Ctrl Pts',(109.20189877539,-1.87444401393148,-15.652454695364));
#62929=CARTESIAN_POINT('Ctrl Pts',(109.249565208391,-1.83253209412259,-15.7004347680384));
#62930=CARTESIAN_POINT('Origin',(109.35,0.,-16.5));
#62931=CARTESIAN_POINT('',(109.35,1.74422220952236,-15.6));
#62932=CARTESIAN_POINT('',(109.35,0.,-15.6));
#62933=CARTESIAN_POINT('',(109.35,1.74422220952236,15.5));
#62934=CARTESIAN_POINT('',(109.35,1.74422220952236,-16.));
#62935=CARTESIAN_POINT('',(109.35,0.,15.5));
#62936=CARTESIAN_POINT('Origin',(109.15,0.,-15.8));
#62937=CARTESIAN_POINT('',(108.95,-1.44913767461896,-16.));
#62938=CARTESIAN_POINT('Ctrl Pts',(108.95,-1.44913767461895,-16.));
#62939=CARTESIAN_POINT('Ctrl Pts',(109.043415355692,-1.58450938593979,-15.9065846443083));
#62940=CARTESIAN_POINT('Ctrl Pts',(109.144875979995,-1.71256291063752,-15.8051240200051));
#62941=CARTESIAN_POINT('Ctrl Pts',(109.249565215576,-1.83253210215195,-15.7004347844244));
#62942=CARTESIAN_POINT('',(108.95,1.44913767461895,-16.));
#62943=CARTESIAN_POINT('',(108.95,0.,-16.));
#62944=CARTESIAN_POINT('',(109.249565208391,1.83253209412259,-15.7004347680384));
#62945=CARTESIAN_POINT('Ctrl Pts',(109.249565215576,1.83253210215195,-15.7004347844244));
#62946=CARTESIAN_POINT('Ctrl Pts',(109.144875979995,1.71256291063752,-15.8051240200051));
#62947=CARTESIAN_POINT('Ctrl Pts',(109.043415355692,1.5845093859398,-15.9065846443082));
#62948=CARTESIAN_POINT('Ctrl Pts',(108.95,1.44913767461895,-16.));
#62949=CARTESIAN_POINT('',(109.450571828096,1.65579187964854,-15.4994281719038));
#62950=CARTESIAN_POINT('Origin',(109.250821963405,1.83142701287898,-16.));
#62951=CARTESIAN_POINT('Ctrl Pts',(109.249565208391,1.83253209412259,-15.7004347680384));
#62952=CARTESIAN_POINT('Ctrl Pts',(109.201898775389,1.87444401393228,-15.6524546953631));
#62953=CARTESIAN_POINT('Ctrl Pts',(109.15164392681,1.91863181623643,-15.5999999999986));
#62954=CARTESIAN_POINT('',(109.732882317017,1.40756322422156,15.5));
#62955=CARTESIAN_POINT('Origin',(109.749178036595,1.83142701287898,-16.));
#62956=CARTESIAN_POINT('',(109.1825212855,1.33317969677524,15.5));
#62957=CARTESIAN_POINT('Origin',(109.5,0.,-16.));
#62958=CARTESIAN_POINT('Origin',(109.5,0.,-15.8));
#62959=CARTESIAN_POINT('Origin',(109.5,0.,-16.));
#62960=CARTESIAN_POINT('Origin',(109.5,0.,-16.));
#62961=CARTESIAN_POINT('Origin',(109.35,0.,15.5));
#62962=CARTESIAN_POINT('Origin',(110.1,0.,19.6));
#62963=CARTESIAN_POINT('',(110.1,-1.22464679914735E-16,20.9));
#62964=CARTESIAN_POINT('Origin',(110.1,0.,21.9));
#62965=CARTESIAN_POINT('Origin',(110.1,1.22464679914735E-16,19.6));
#62966=CARTESIAN_POINT('Ctrl Pts',(110.957496466316,-0.968609346005826,
17.2));
#62967=CARTESIAN_POINT('Ctrl Pts',(110.666585330308,-0.993729619858369,
17.2));
#62968=CARTESIAN_POINT('Ctrl Pts',(110.369405244968,-0.994987437106615,
17.2));
#62969=CARTESIAN_POINT('Ctrl Pts',(109.584606004541,-0.994987437106615,
17.2));
#62970=CARTESIAN_POINT('Ctrl Pts',(108.966168883834,-1.00163012723263,17.2));
#62971=CARTESIAN_POINT('Ctrl Pts',(108.351640706405,-0.750967734840807,
17.2));
#62972=CARTESIAN_POINT('Ctrl Pts',(108.198421877032,-0.660471858983854,
17.2));
#62973=CARTESIAN_POINT('Ctrl Pts',(108.013855167537,-0.484337954844702,
17.2));
#62974=CARTESIAN_POINT('Ctrl Pts',(107.937850648849,-0.38109745127946,17.2));
#62975=CARTESIAN_POINT('Ctrl Pts',(107.858447096036,-0.19916364867032,17.2));
#62976=CARTESIAN_POINT('Ctrl Pts',(107.835049669419,-0.0916730147518283,
17.2));
#62977=CARTESIAN_POINT('Ctrl Pts',(107.835049669419,0.0916730147518283,
17.2));
#62978=CARTESIAN_POINT('Ctrl Pts',(107.858447096036,0.19916364867032,17.2));
#62979=CARTESIAN_POINT('Ctrl Pts',(107.937850648849,0.38109745127946,17.2));
#62980=CARTESIAN_POINT('Ctrl Pts',(108.013855167537,0.484337954844702,17.2));
#62981=CARTESIAN_POINT('Ctrl Pts',(108.198421877032,0.660471858983854,17.2));
#62982=CARTESIAN_POINT('Ctrl Pts',(108.351640706405,0.750967734840807,17.2));
#62983=CARTESIAN_POINT('Ctrl Pts',(108.966168883834,1.00163012723263,17.2));
#62984=CARTESIAN_POINT('Ctrl Pts',(109.584606004541,0.994987437106615,17.2));
#62985=CARTESIAN_POINT('Ctrl Pts',(110.1,0.994987437106615,17.2));
#62986=CARTESIAN_POINT('Ctrl Pts',(110.369405244968,0.994987437106615,17.2));
#62987=CARTESIAN_POINT('Ctrl Pts',(110.666585330308,0.993729619858367,17.2));
#62988=CARTESIAN_POINT('Ctrl Pts',(110.957496466316,0.968609346005826,17.2));
#62989=CARTESIAN_POINT('Origin',(109.5,0.,17.2));
#71609=UNCERTAINTY_MEASURE_WITH_UNIT(LENGTH_MEASURE(0.01),#71629,
'DISTANCE_ACCURACY_VALUE',
'Maximum model space distance between geometric entities at asserted c
onnectivities');
#71613=UNCERTAINTY_MEASURE_WITH_UNIT(LENGTH_MEASURE(0.01),#71629,
'DISTANCE_ACCURACY_VALUE',
'Maximum model space distance between geometric entities at asserted c
onnectivities');
#71624=(
GEOMETRIC_REPRESENTATION_CONTEXT(3)
GLOBAL_UNCERTAINTY_ASSIGNED_CONTEXT((#71609))
GLOBAL_UNIT_ASSIGNED_CONTEXT((#71629,#71631,#71632))
REPRESENTATION_CONTEXT('','3D')
);
#71628=(
GEOMETRIC_REPRESENTATION_CONTEXT(3)
GLOBAL_UNCERTAINTY_ASSIGNED_CONTEXT((#71613))
GLOBAL_UNIT_ASSIGNED_CONTEXT((#71629,#71631,#71632))
REPRESENTATION_CONTEXT('','3D')
);
#71629=(
LENGTH_UNIT()
NAMED_UNIT(*)
SI_UNIT(.MILLI.,.METRE.)
);
#71631=(
NAMED_UNIT(*)
PLANE_ANGLE_UNIT()
SI_UNIT($,.RADIAN.)
);
#71632=(
NAMED_UNIT(*)
SI_UNIT($,.STERADIAN.)
SOLID_ANGLE_UNIT()
);
#71643=SHAPE_DEFINITION_REPRESENTATION(#71657,#71692);
#71657=PRODUCT_DEFINITION_SHAPE('',$,#71707);
#71692=SHAPE_REPRESENTATION('',(#37185),#71624);
#71696=PRODUCT_DEFINITION_CONTEXT('part definition',#71740,'design');
#71707=PRODUCT_DEFINITION('2026-10-25-00-23-55-849',
'13_Cotter_Pin_5-32x1-1-4',#71721,#71696);
#71721=PRODUCT_DEFINITION_FORMATION('',$,#71752);
#71740=APPLICATION_CONTEXT(
'Core Data for Automotive Mechanical Design Process');
#71741=PRODUCT_CONTEXT('part definition',#71740,'mechanical');
#71752=PRODUCT('2026-10-25-00-23-55-849','13_Cotter_Pin_5-32x1-1-4',$,(#71741));
#71812=COLOUR_RGB('Grey',0.48,0.52,0.57);
#71813=FILL_AREA_STYLE_COLOUR('',#71812);
#71814=FILL_AREA_STYLE('',(#71813));
#71815=SURFACE_STYLE_FILL_AREA(#71814);
#71816=SURFACE_SIDE_STYLE('',(#71815));
#71817=SURFACE_STYLE_USAGE(.BOTH.,#71816);
#71818=PRESENTATION_STYLE_ASSIGNMENT((#71817));
ENDSEC;
END-ISO-10303-21;
